ISO-10303-21;
HEADER;
/* Generated by software containing ST-Developer
 * from STEP Tools, Inc. (www.steptools.com) 
 */

FILE_DESCRIPTION(
/* description */ ('PAT-083'),
/* implementation_level */ '2;1');

FILE_NAME(
/* name */ 'Base.step',
/* time_stamp */ '2026-10-29T20:18:00-07:00',
/* author */ (''),
/* organization */ (''),
/* preprocessor_version */ 'ST-DEVELOPER v20.2',
/* originating_system */ 'Autodesk Translation Framework v15.17.0.0',
/* authorisation */ '');

FILE_SCHEMA (('AUTOMOTIVE_DESIGN { 1 0 10303 214 3 1 1 }'));
ENDSEC;

DATA;
#10=MECHANICAL_DESIGN_GEOMETRIC_PRESENTATION_REPRESENTATION('',(#229),#8428);
#181=SHAPE_REPRESENTATION_RELATIONSHIP('SRR','None',#8515,#205);
#205=ADVANCED_BREP_SHAPE_REPRESENTATION('',(#253),#8404);
#229=STYLED_ITEM('',(#8684),#253);
#253=MANIFOLD_SOLID_BREP('Body1',#3675);
#275=FACE_BOUND('',#735,.T.);
#276=FACE_BOUND('',#736,.T.);
#277=FACE_BOUND('',#738,.T.);
#278=FACE_BOUND('',#739,.T.);
#356=PLANE('',#3974);
#357=PLANE('',#3975);
#358=PLANE('',#3976);
#359=PLANE('',#3977);
#360=PLANE('',#3978);
#361=PLANE('',#3979);
#495=FACE_OUTER_BOUND('',#728,.T.);
#496=FACE_OUTER_BOUND('',#729,.T.);
#497=FACE_OUTER_BOUND('',#730,.T.);
#498=FACE_OUTER_BOUND('',#731,.T.);
#499=FACE_OUTER_BOUND('',#732,.T.);
#500=FACE_OUTER_BOUND('',#733,.T.);
#501=FACE_OUTER_BOUND('',#734,.T.);
#502=FACE_OUTER_BOUND('',#737,.T.);
#728=EDGE_LOOP('',(#2458,#2459,#2460,#2461));
#729=EDGE_LOOP('',(#2462,#2463,#2464,#2465));
#730=EDGE_LOOP('',(#2466,#2467,#2468,#2469));
#731=EDGE_LOOP('',(#2470,#2471,#2472,#2473));
#732=EDGE_LOOP('',(#2474,#2475,#2476,#2477));
#733=EDGE_LOOP('',(#2478,#2479,#2480,#2481));
#734=EDGE_LOOP('',(#2482,#2483,#2484,#2485));
#735=EDGE_LOOP('',(#2486));
#736=EDGE_LOOP('',(#2487));
#737=EDGE_LOOP('',(#2488,#2489,#2490,#2491));
#738=EDGE_LOOP('',(#2492));
#739=EDGE_LOOP('',(#2493));
#1042=LINE('',#5626,#1286);
#1043=LINE('',#5632,#1287);
#1044=LINE('',#5637,#1288);
#1045=LINE('',#5639,#1289);
#1046=LINE('',#5641,#1290);
#1047=LINE('',#5642,#1291);
#1048=LINE('',#5645,#1292);
#1049=LINE('',#5647,#1293);
#1050=LINE('',#5648,#1294);
#1051=LINE('',#5651,#1295);
#1052=LINE('',#5653,#1296);
#1053=LINE('',#5654,#1297);
#1054=LINE('',#5656,#1298);
#1055=LINE('',#5657,#1299);
#1286=VECTOR('',#4444,0.225);
#1287=VECTOR('',#4451,0.225);
#1288=VECTOR('',#4456,1.);
#1289=VECTOR('',#4457,1.);
#1290=VECTOR('',#4458,1.);
#1291=VECTOR('',#4459,1.);
#1292=VECTOR('',#4462,1.);
#1293=VECTOR('',#4463,1.);
#1294=VECTOR('',#4464,1.);
#1295=VECTOR('',#4467,1.);
#1296=VECTOR('',#4468,1.);
#1297=VECTOR('',#4469,1.);
#1298=VECTOR('',#4472,1.);
#1299=VECTOR('',#4473,1.);
#1530=CIRCLE('',#3969,0.225);
#1531=CIRCLE('',#3970,0.225);
#1532=CIRCLE('',#3972,0.225);
#1533=CIRCLE('',#3973,0.225);
#1713=VERTEX_POINT('',#5623);
#1714=VERTEX_POINT('',#5625);
#1715=VERTEX_POINT('',#5629);
#1716=VERTEX_POINT('',#5631);
#1717=VERTEX_POINT('',#5635);
#1718=VERTEX_POINT('',#5636);
#1719=VERTEX_POINT('',#5638);
#1720=VERTEX_POINT('',#5640);
#1721=VERTEX_POINT('',#5644);
#1722=VERTEX_POINT('',#5646);
#1723=VERTEX_POINT('',#5650);
#1724=VERTEX_POINT('',#5652);
#2005=EDGE_CURVE('',#1713,#1713,#1530,.T.);
#2006=EDGE_CURVE('',#1713,#1714,#1042,.T.);
#2007=EDGE_CURVE('',#1714,#1714,#1531,.T.);
#2008=EDGE_CURVE('',#1715,#1715,#1532,.T.);
#2009=EDGE_CURVE('',#1715,#1716,#1043,.T.);
#2010=EDGE_CURVE('',#1716,#1716,#1533,.T.);
#2011=EDGE_CURVE('',#1717,#1718,#1044,.T.);
#2012=EDGE_CURVE('',#1718,#1719,#1045,.T.);
#2013=EDGE_CURVE('',#1720,#1719,#1046,.T.);
#2014=EDGE_CURVE('',#1717,#1720,#1047,.T.);
#2015=EDGE_CURVE('',#1721,#1717,#1048,.T.);
#2016=EDGE_CURVE('',#1722,#1720,#1049,.T.);
#2017=EDGE_CURVE('',#1721,#1722,#1050,.T.);
#2018=EDGE_CURVE('',#1723,#1721,#1051,.T.);
#2019=EDGE_CURVE('',#1724,#1722,#1052,.T.);
#2020=EDGE_CURVE('',#1723,#1724,#1053,.T.);
#2021=EDGE_CURVE('',#1718,#1723,#1054,.T.);
#2022=EDGE_CURVE('',#1719,#1724,#1055,.T.);
#2458=ORIENTED_EDGE('',*,*,#2005,.F.);
#2459=ORIENTED_EDGE('',*,*,#2006,.T.);
#2460=ORIENTED_EDGE('',*,*,#2007,.F.);
#2461=ORIENTED_EDGE('',*,*,#2006,.F.);
#2462=ORIENTED_EDGE('',*,*,#2008,.F.);
#2463=ORIENTED_EDGE('',*,*,#2009,.T.);
#2464=ORIENTED_EDGE('',*,*,#2010,.F.);
#2465=ORIENTED_EDGE('',*,*,#2009,.F.);
#2466=ORIENTED_EDGE('',*,*,#2011,.T.);
#2467=ORIENTED_EDGE('',*,*,#2012,.T.);
#2468=ORIENTED_EDGE('',*,*,#2013,.F.);
#2469=ORIENTED_EDGE('',*,*,#2014,.F.);
#2470=ORIENTED_EDGE('',*,*,#2015,.T.);
#2471=ORIENTED_EDGE('',*,*,#2014,.T.);
#2472=ORIENTED_EDGE('',*,*,#2016,.F.);
#2473=ORIENTED_EDGE('',*,*,#2017,.F.);
#2474=ORIENTED_EDGE('',*,*,#2018,.T.);
#2475=ORIENTED_EDGE('',*,*,#2017,.T.);
#2476=ORIENTED_EDGE('',*,*,#2019,.F.);
#2477=ORIENTED_EDGE('',*,*,#2020,.F.);
#2478=ORIENTED_EDGE('',*,*,#2021,.T.);
#2479=ORIENTED_EDGE('',*,*,#2020,.T.);
#2480=ORIENTED_EDGE('',*,*,#2022,.F.);
#2481=ORIENTED_EDGE('',*,*,#2012,.F.);
#2482=ORIENTED_EDGE('',*,*,#2022,.T.);
#2483=ORIENTED_EDGE('',*,*,#2019,.T.);
#2484=ORIENTED_EDGE('',*,*,#2016,.T.);
#2485=ORIENTED_EDGE('',*,*,#2013,.T.);
#2486=ORIENTED_EDGE('',*,*,#2007,.T.);
#2487=ORIENTED_EDGE('',*,*,#2010,.T.);
#2488=ORIENTED_EDGE('',*,*,#2021,.F.);
#2489=ORIENTED_EDGE('',*,*,#2011,.F.);
#2490=ORIENTED_EDGE('',*,*,#2015,.F.);
#2491=ORIENTED_EDGE('',*,*,#2018,.F.);
#2492=ORIENTED_EDGE('',*,*,#2005,.T.);
#2493=ORIENTED_EDGE('',*,*,#2008,.T.);
#3364=CYLINDRICAL_SURFACE('',#3968,0.225);
#3365=CYLINDRICAL_SURFACE('',#3971,0.225);
#3442=ADVANCED_FACE('',(#495),#3364,.F.);
#3443=ADVANCED_FACE('',(#496),#3365,.F.);
#3444=ADVANCED_FACE('',(#497),#356,.T.);
#3445=ADVANCED_FACE('',(#498),#357,.T.);
#3446=ADVANCED_FACE('',(#499),#358,.T.);
#3447=ADVANCED_FACE('',(#500),#359,.T.);
#3448=ADVANCED_FACE('',(#501,#275,#276),#360,.T.);
#3449=ADVANCED_FACE('',(#502,#277,#278),#361,.F.);
#3675=CLOSED_SHELL('',(#3442,#3443,#3444,#3445,#3446,#3447,#3448,#3449));
#3967=AXIS2_PLACEMENT_3D('',#5621,#4438,#4439);
#3968=AXIS2_PLACEMENT_3D('',#5622,#4440,#4441);
#3969=AXIS2_PLACEMENT_3D('',#5624,#4442,#4443);
#3970=AXIS2_PLACEMENT_3D('',#5627,#4445,#4446);
#3971=AXIS2_PLACEMENT_3D('',#5628,#4447,#4448);
#3972=AXIS2_PLACEMENT_3D('',#5630,#4449,#4450);
#3973=AXIS2_PLACEMENT_3D('',#5633,#4452,#4453);
#3974=AXIS2_PLACEMENT_3D('',#5634,#4454,#4455);
#3975=AXIS2_PLACEMENT_3D('',#5643,#4460,#4461);
#3976=AXIS2_PLACEMENT_3D('',#5649,#4465,#4466);
#3977=AXIS2_PLACEMENT_3D('',#5655,#4470,#4471);
#3978=AXIS2_PLACEMENT_3D('',#5658,#4474,#4475);
#3979=AXIS2_PLACEMENT_3D('',#5659,#4476,#4477);
#4438=DIRECTION('axis',(0.,0.,1.));
#4439=DIRECTION('refdir',(1.,0.,0.));
#4440=DIRECTION('center_axis',(0.,0.,1.));
#4441=DIRECTION('ref_axis',(1.,0.,0.));
#4442=DIRECTION('center_axis',(0.,0.,1.));
#4443=DIRECTION('ref_axis',(1.,0.,0.));
#4444=DIRECTION('',(0.,0.,1.));
#4445=DIRECTION('center_axis',(0.,0.,-1.));
#4446=DIRECTION('ref_axis',(1.,0.,0.));
#4447=DIRECTION('center_axis',(0.,0.,1.));
#4448=DIRECTION('ref_axis',(1.,0.,0.));
#4449=DIRECTION('center_axis',(0.,0.,1.));
#4450=DIRECTION('ref_axis',(1.,0.,0.));
#4451=DIRECTION('',(0.,0.,1.));
#4452=DIRECTION('center_axis',(0.,0.,-1.));
#4453=DIRECTION('ref_axis',(1.,0.,0.));
#4454=DIRECTION('center_axis',(0.,1.,0.));
#4455=DIRECTION('ref_axis',(-1.,0.,0.));
#4456=DIRECTION('',(-1.,0.,0.));
#4457=DIRECTION('',(0.,0.,1.));
#4458=DIRECTION('',(-1.,0.,0.));
#4459=DIRECTION('',(0.,0.,1.));
#4460=DIRECTION('center_axis',(1.,0.,0.));
#4461=DIRECTION('ref_axis',(0.,1.,0.));
#4462=DIRECTION('',(0.,1.,0.));
#4463=DIRECTION('',(0.,1.,0.));
#4464=DIRECTION('',(0.,0.,1.));
#4465=DIRECTION('center_axis',(0.,-1.,0.));
#4466=DIRECTION('ref_axis',(1.,0.,0.));
#4467=DIRECTION('',(1.,0.,0.));
#4468=DIRECTION('',(1.,0.,0.));
#4469=DIRECTION('',(0.,0.,1.));
#4470=DIRECTION('center_axis',(-1.,0.,0.));
#4471=DIRECTION('ref_axis',(0.,-1.,0.));
#4472=DIRECTION('',(0.,-1.,0.));
#4473=DIRECTION('',(0.,-1.,0.));
#4474=DIRECTION('center_axis',(0.,0.,1.));
#4475=DIRECTION('ref_axis',(1.,0.,0.));
#4476=DIRECTION('center_axis',(0.,0.,1.));
#4477=DIRECTION('ref_axis',(1.,0.,0.));
#5621=CARTESIAN_POINT('',(0.,0.,0.));
#5622=CARTESIAN_POINT('Origin',(0.,-3.,-0.1));
#5623=CARTESIAN_POINT('',(-0.225,-3.,0.));
#5624=CARTESIAN_POINT('Origin',(0.,-3.,0.));
#5625=CARTESIAN_POINT('',(-0.225,-3.,0.6));
#5626=CARTESIAN_POINT('',(-0.225,-3.,-0.1));
#5627=CARTESIAN_POINT('Origin',(0.,-3.,0.6));
#5628=CARTESIAN_POINT('Origin',(0.,3.,-0.1));
#5629=CARTESIAN_POINT('',(-0.225,3.,0.));
#5630=CARTESIAN_POINT('Origin',(0.,3.,0.));
#5631=CARTESIAN_POINT('',(-0.225,3.,0.6));
#5632=CARTESIAN_POINT('',(-0.225,3.,-0.1));
#5633=CARTESIAN_POINT('Origin',(0.,3.,0.6));
#5634=CARTESIAN_POINT('Origin',(6.,4.5,0.));
#5635=CARTESIAN_POINT('',(6.,4.5,0.));
#5636=CARTESIAN_POINT('',(-6.,4.5,0.));
#5637=CARTESIAN_POINT('',(6.,4.5,0.));
#5638=CARTESIAN_POINT('',(-6.,4.5,0.6));
#5639=CARTESIAN_POINT('',(-6.,4.5,0.));
#5640=CARTESIAN_POINT('',(6.,4.5,0.6));
#5641=CARTESIAN_POINT('',(6.,4.5,0.6));
#5642=CARTESIAN_POINT('',(6.,4.5,0.));
#5643=CARTESIAN_POINT('Origin',(6.,-4.5,0.));
#5644=CARTESIAN_POINT('',(6.,-4.5,0.));
#5645=CARTESIAN_POINT('',(6.,-4.5,0.));
#5646=CARTESIAN_POINT('',(6.,-4.5,0.6));
#5647=CARTESIAN_POINT('',(6.,-4.5,0.6));
#5648=CARTESIAN_POINT('',(6.,-4.5,0.));
#5649=CARTESIAN_POINT('Origin',(-6.,-4.5,0.));
#5650=CARTESIAN_POINT('',(-6.,-4.5,0.));
#5651=CARTESIAN_POINT('',(-6.,-4.5,0.));
#5652=CARTESIAN_POINT('',(-6.,-4.5,0.6));
#5653=CARTESIAN_POINT('',(-6.,-4.5,0.6));
#5654=CARTESIAN_POINT('',(-6.,-4.5,0.));
#5655=CARTESIAN_POINT('Origin',(-6.,4.5,0.));
#5656=CARTESIAN_POINT('',(-6.,4.5,0.));
#5657=CARTESIAN_POINT('',(-6.,4.5,0.6));
#5658=CARTESIAN_POINT('Origin',(0.,0.,0.6));
#5659=CARTESIAN_POINT('Origin',(0.,0.,0.));
#8378=UNCERTAINTY_MEASURE_WITH_UNIT(LENGTH_MEASURE(0.001),#8429,
'DISTANCE_ACCURACY_VALUE',
'Maximum model space distance between geometric entities at asserted c
onnectivities');
#8402=UNCERTAINTY_MEASURE_WITH_UNIT(LENGTH_MEASURE(0.001),#8429,
'DISTANCE_ACCURACY_VALUE',
'Maximum model space distance between geometric entities at asserted c
onnectivities');
#8404=(
GEOMETRIC_REPRESENTATION_CONTEXT(3)
GLOBAL_UNCERTAINTY_ASSIGNED_CONTEXT((#8378))
GLOBAL_UNIT_ASSIGNED_CONTEXT((#8429,#8431,#8432))
REPRESENTATION_CONTEXT('','3D')
);
#8428=(
GEOMETRIC_REPRESENTATION_CONTEXT(3)
GLOBAL_UNCERTAINTY_ASSIGNED_CONTEXT((#8402))
GLOBAL_UNIT_ASSIGNED_CONTEXT((#8429,#8431,#8432))
REPRESENTATION_CONTEXT('','3D')
);
#8429=(
LENGTH_UNIT()
NAMED_UNIT(*)
SI_UNIT(.CENTI.,.METRE.)
);
#8431=(
NAMED_UNIT(*)
PLANE_ANGLE_UNIT()
SI_UNIT($,.RADIAN.)
);
#8432=(
NAMED_UNIT(*)
SI_UNIT($,.STERADIAN.)
SOLID_ANGLE_UNIT()
);
#8434=SHAPE_DEFINITION_REPRESENTATION(#8459,#8515);
#8459=PRODUCT_DEFINITION_SHAPE('',$,#8541);
#8515=SHAPE_REPRESENTATION('',(#3967),#8404);
#8539=PRODUCT_DEFINITION_CONTEXT('part definition',#8616,'design');
#8541=PRODUCT_DEFINITION('Base','Base',#8566,#8539);
#8566=PRODUCT_DEFINITION_FORMATION('',$,#8619);
#8616=APPLICATION_CONTEXT(
'Core Data for Automotive Mechanical Design Process');
#8617=PRODUCT_CONTEXT('part definition',#8616,'mechanical');
#8619=PRODUCT('Base','Base','Base',(#8617));
#8678=COLOUR_RGB('Dark Blue',0.08,0.2,0.34);
#8679=FILL_AREA_STYLE_COLOUR('',#8678);
#8680=FILL_AREA_STYLE('',(#8679));
#8681=SURFACE_STYLE_FILL_AREA(#8680);
#8682=SURFACE_SIDE_STYLE('',(#8681));
#8683=SURFACE_STYLE_USAGE(.BOTH.,#8682);
#8684=PRESENTATION_STYLE_ASSIGNMENT((#8683));
ENDSEC;
END-ISO-10303-21;
